ISO-10303-21;
HEADER;
/* Generated by software containing ST-Developer
 * from STEP Tools, Inc. (www.steptools.com) 
 */

FILE_DESCRIPTION(
/* description */ ('PAT-091'),
/* implementation_level */ '2;1');

FILE_NAME(
/* name */ 'Linear bearing keeper (3).step',
/* time_stamp */ '2026-10-27T15:34:44-07:00',
/* author */ (''),
/* organization */ (''),
/* preprocessor_version */ 'ST-DEVELOPER v20.2',
/* originating_system */ 'Autodesk Translation Framework v15.17.0.0',
/* authorisation */ '');

FILE_SCHEMA (('AUTOMOTIVE_DESIGN { 1 0 10303 214 3 1 1 }'));
ENDSEC;

DATA;
#10=MECHANICAL_DESIGN_GEOMETRIC_PRESENTATION_REPRESENTATION('',(#1015),#25100);
#795=SHAPE_REPRESENTATION_RELATIONSHIP('SRR','None',#25559,#905);
#905=ADVANCED_BREP_SHAPE_REPRESENTATION('',(#1137),#25029);
#1015=STYLED_ITEM('',(#26191),#1137);
#1137=MANIFOLD_SOLID_BREP('Body1',#13294);
#1446=FACE_BOUND('',#3472,.T.);
#1447=FACE_BOUND('',#3475,.T.);
#1448=FACE_BOUND('',#3484,.T.);
#1449=FACE_BOUND('',#3485,.T.);
#1450=FACE_BOUND('',#3486,.T.);
#1451=FACE_BOUND('',#3488,.T.);
#1452=FACE_BOUND('',#3489,.T.);
#1453=FACE_BOUND('',#3490,.T.);
#1837=PLANE('',#15313);
#1838=PLANE('',#15318);
#1839=PLANE('',#15327);
#1840=PLANE('',#15328);
#1841=PLANE('',#15329);
#1842=PLANE('',#15330);
#1843=PLANE('',#15331);
#1844=PLANE('',#15332);
#2421=FACE_OUTER_BOUND('',#3470,.T.);
#2422=FACE_OUTER_BOUND('',#3471,.T.);
#2423=FACE_OUTER_BOUND('',#3473,.T.);
#2424=FACE_OUTER_BOUND('',#3474,.T.);
#2425=FACE_OUTER_BOUND('',#3476,.T.);
#2426=FACE_OUTER_BOUND('',#3477,.T.);
#2427=FACE_OUTER_BOUND('',#3478,.T.);
#2428=FACE_OUTER_BOUND('',#3479,.T.);
#2429=FACE_OUTER_BOUND('',#3480,.T.);
#2430=FACE_OUTER_BOUND('',#3481,.T.);
#2431=FACE_OUTER_BOUND('',#3482,.T.);
#2432=FACE_OUTER_BOUND('',#3483,.T.);
#2433=FACE_OUTER_BOUND('',#3487,.T.);
#3470=EDGE_LOOP('',(#10440,#10441,#10442,#10443));
#3471=EDGE_LOOP('',(#10444));
#3472=EDGE_LOOP('',(#10445));
#3473=EDGE_LOOP('',(#10446,#10447,#10448,#10449));
#3474=EDGE_LOOP('',(#10450));
#3475=EDGE_LOOP('',(#10451));
#3476=EDGE_LOOP('',(#10452,#10453,#10454,#10455));
#3477=EDGE_LOOP('',(#10456,#10457,#10458,#10459));
#3478=EDGE_LOOP('',(#10460,#10461,#10462,#10463));
#3479=EDGE_LOOP('',(#10464,#10465,#10466,#10467));
#3480=EDGE_LOOP('',(#10468,#10469,#10470,#10471));
#3481=EDGE_LOOP('',(#10472,#10473,#10474,#10475));
#3482=EDGE_LOOP('',(#10476,#10477,#10478,#10479));
#3483=EDGE_LOOP('',(#10480,#10481,#10482,#10483));
#3484=EDGE_LOOP('',(#10484));
#3485=EDGE_LOOP('',(#10485));
#3486=EDGE_LOOP('',(#10486));
#3487=EDGE_LOOP('',(#10487,#10488,#10489,#10490));
#3488=EDGE_LOOP('',(#10491));
#3489=EDGE_LOOP('',(#10492));
#3490=EDGE_LOOP('',(#10493));
#4539=LINE('',#22633,#5279);
#4540=LINE('',#22642,#5280);
#4541=LINE('',#22651,#5281);
#4542=LINE('',#22655,#5282);
#4543=LINE('',#22659,#5283);
#4544=LINE('',#22664,#5284);
#4545=LINE('',#22666,#5285);
#4546=LINE('',#22668,#5286);
#4547=LINE('',#22669,#5287);
#4548=LINE('',#22672,#5288);
#4549=LINE('',#22674,#5289);
#4550=LINE('',#22675,#5290);
#4551=LINE('',#22678,#5291);
#4552=LINE('',#22680,#5292);
#4553=LINE('',#22681,#5293);
#4554=LINE('',#22683,#5294);
#4555=LINE('',#22684,#5295);
#5279=VECTOR('',#18337,1.04);
#5280=VECTOR('',#18348,1.04);
#5281=VECTOR('',#18359,0.65);
#5282=VECTOR('',#18364,0.800000000000001);
#5283=VECTOR('',#18369,0.800000000000001);
#5284=VECTOR('',#18374,1.);
#5285=VECTOR('',#18375,1.);
#5286=VECTOR('',#18376,1.);
#5287=VECTOR('',#18377,1.);
#5288=VECTOR('',#18380,1.);
#5289=VECTOR('',#18381,1.);
#5290=VECTOR('',#18382,1.);
#5291=VECTOR('',#18385,1.);
#5292=VECTOR('',#18386,1.);
#5293=VECTOR('',#18387,1.);
#5294=VECTOR('',#18390,1.);
#5295=VECTOR('',#18391,1.);
#5921=CIRCLE('',#15311,1.04);
#5922=CIRCLE('',#15312,1.04);
#5923=CIRCLE('',#15314,0.800000000000001);
#5924=CIRCLE('',#15316,1.04);
#5925=CIRCLE('',#15317,1.04);
#5926=CIRCLE('',#15319,0.800000000000001);
#5927=CIRCLE('',#15321,0.65);
#5928=CIRCLE('',#15322,0.65);
#5929=CIRCLE('',#15324,0.800000000000001);
#5930=CIRCLE('',#15326,0.800000000000001);
#6870=VERTEX_POINT('',#22630);
#6871=VERTEX_POINT('',#22632);
#6872=VERTEX_POINT('',#22636);
#6873=VERTEX_POINT('',#22639);
#6874=VERTEX_POINT('',#22641);
#6875=VERTEX_POINT('',#22645);
#6876=VERTEX_POINT('',#22648);
#6877=VERTEX_POINT('',#22650);
#6878=VERTEX_POINT('',#22654);
#6879=VERTEX_POINT('',#22658);
#6880=VERTEX_POINT('',#22662);
#6881=VERTEX_POINT('',#22663);
#6882=VERTEX_POINT('',#22665);
#6883=VERTEX_POINT('',#22667);
#6884=VERTEX_POINT('',#22671);
#6885=VERTEX_POINT('',#22673);
#6886=VERTEX_POINT('',#22677);
#6887=VERTEX_POINT('',#22679);
#8155=EDGE_CURVE('',#6870,#6870,#5921,.T.);
#8156=EDGE_CURVE('',#6870,#6871,#4539,.T.);
#8157=EDGE_CURVE('',#6871,#6871,#5922,.T.);
#8158=EDGE_CURVE('',#6872,#6872,#5923,.T.);
#8159=EDGE_CURVE('',#6873,#6873,#5924,.T.);
#8160=EDGE_CURVE('',#6873,#6874,#4540,.T.);
#8161=EDGE_CURVE('',#6874,#6874,#5925,.T.);
#8162=EDGE_CURVE('',#6875,#6875,#5926,.T.);
#8163=EDGE_CURVE('',#6876,#6876,#5927,.T.);
#8164=EDGE_CURVE('',#6876,#6877,#4541,.T.);
#8165=EDGE_CURVE('',#6877,#6877,#5928,.T.);
#8166=EDGE_CURVE('',#6875,#6878,#4542,.T.);
#8167=EDGE_CURVE('',#6878,#6878,#5929,.T.);
#8168=EDGE_CURVE('',#6872,#6879,#4543,.T.);
#8169=EDGE_CURVE('',#6879,#6879,#5930,.T.);
#8170=EDGE_CURVE('',#6880,#6881,#4544,.T.);
#8171=EDGE_CURVE('',#6881,#6882,#4545,.T.);
#8172=EDGE_CURVE('',#6883,#6882,#4546,.T.);
#8173=EDGE_CURVE('',#6880,#6883,#4547,.T.);
#8174=EDGE_CURVE('',#6884,#6880,#4548,.T.);
#8175=EDGE_CURVE('',#6885,#6883,#4549,.T.);
#8176=EDGE_CURVE('',#6884,#6885,#4550,.T.);
#8177=EDGE_CURVE('',#6886,#6884,#4551,.T.);
#8178=EDGE_CURVE('',#6887,#6885,#4552,.T.);
#8179=EDGE_CURVE('',#6886,#6887,#4553,.T.);
#8180=EDGE_CURVE('',#6881,#6886,#4554,.T.);
#8181=EDGE_CURVE('',#6882,#6887,#4555,.T.);
#10440=ORIENTED_EDGE('',*,*,#8155,.F.);
#10441=ORIENTED_EDGE('',*,*,#8156,.T.);
#10442=ORIENTED_EDGE('',*,*,#8157,.T.);
#10443=ORIENTED_EDGE('',*,*,#8156,.F.);
#10444=ORIENTED_EDGE('',*,*,#8157,.F.);
#10445=ORIENTED_EDGE('',*,*,#8158,.F.);
#10446=ORIENTED_EDGE('',*,*,#8159,.F.);
#10447=ORIENTED_EDGE('',*,*,#8160,.T.);
#10448=ORIENTED_EDGE('',*,*,#8161,.T.);
#10449=ORIENTED_EDGE('',*,*,#8160,.F.);
#10450=ORIENTED_EDGE('',*,*,#8161,.F.);
#10451=ORIENTED_EDGE('',*,*,#8162,.F.);
#10452=ORIENTED_EDGE('',*,*,#8163,.F.);
#10453=ORIENTED_EDGE('',*,*,#8164,.T.);
#10454=ORIENTED_EDGE('',*,*,#8165,.F.);
#10455=ORIENTED_EDGE('',*,*,#8164,.F.);
#10456=ORIENTED_EDGE('',*,*,#8162,.T.);
#10457=ORIENTED_EDGE('',*,*,#8166,.T.);
#10458=ORIENTED_EDGE('',*,*,#8167,.F.);
#10459=ORIENTED_EDGE('',*,*,#8166,.F.);
#10460=ORIENTED_EDGE('',*,*,#8158,.T.);
#10461=ORIENTED_EDGE('',*,*,#8168,.T.);
#10462=ORIENTED_EDGE('',*,*,#8169,.F.);
#10463=ORIENTED_EDGE('',*,*,#8168,.F.);
#10464=ORIENTED_EDGE('',*,*,#8170,.T.);
#10465=ORIENTED_EDGE('',*,*,#8171,.T.);
#10466=ORIENTED_EDGE('',*,*,#8172,.F.);
#10467=ORIENTED_EDGE('',*,*,#8173,.F.);
#10468=ORIENTED_EDGE('',*,*,#8174,.T.);
#10469=ORIENTED_EDGE('',*,*,#8173,.T.);
#10470=ORIENTED_EDGE('',*,*,#8175,.F.);
#10471=ORIENTED_EDGE('',*,*,#8176,.F.);
#10472=ORIENTED_EDGE('',*,*,#8177,.T.);
#10473=ORIENTED_EDGE('',*,*,#8176,.T.);
#10474=ORIENTED_EDGE('',*,*,#8178,.F.);
#10475=ORIENTED_EDGE('',*,*,#8179,.F.);
#10476=ORIENTED_EDGE('',*,*,#8180,.T.);
#10477=ORIENTED_EDGE('',*,*,#8179,.T.);
#10478=ORIENTED_EDGE('',*,*,#8181,.F.);
#10479=ORIENTED_EDGE('',*,*,#8171,.F.);
#10480=ORIENTED_EDGE('',*,*,#8181,.T.);
#10481=ORIENTED_EDGE('',*,*,#8178,.T.);
#10482=ORIENTED_EDGE('',*,*,#8175,.T.);
#10483=ORIENTED_EDGE('',*,*,#8172,.T.);
#10484=ORIENTED_EDGE('',*,*,#8165,.T.);
#10485=ORIENTED_EDGE('',*,*,#8167,.T.);
#10486=ORIENTED_EDGE('',*,*,#8169,.T.);
#10487=ORIENTED_EDGE('',*,*,#8180,.F.);
#10488=ORIENTED_EDGE('',*,*,#8170,.F.);
#10489=ORIENTED_EDGE('',*,*,#8174,.F.);
#10490=ORIENTED_EDGE('',*,*,#8177,.F.);
#10491=ORIENTED_EDGE('',*,*,#8155,.T.);
#10492=ORIENTED_EDGE('',*,*,#8159,.T.);
#10493=ORIENTED_EDGE('',*,*,#8163,.T.);
#12228=CYLINDRICAL_SURFACE('',#15310,1.04);
#12229=CYLINDRICAL_SURFACE('',#15315,1.04);
#12230=CYLINDRICAL_SURFACE('',#15320,0.65);
#12231=CYLINDRICAL_SURFACE('',#15323,0.800000000000001);
#12232=CYLINDRICAL_SURFACE('',#15325,0.800000000000001);
#12788=ADVANCED_FACE('',(#2421),#12228,.T.);
#12789=ADVANCED_FACE('',(#2422,#1446),#1837,.F.);
#12790=ADVANCED_FACE('',(#2423),#12229,.T.);
#12791=ADVANCED_FACE('',(#2424,#1447),#1838,.F.);
#12792=ADVANCED_FACE('',(#2425),#12230,.F.);
#12793=ADVANCED_FACE('',(#2426),#12231,.F.);
#12794=ADVANCED_FACE('',(#2427),#12232,.F.);
#12795=ADVANCED_FACE('',(#2428),#1839,.T.);
#12796=ADVANCED_FACE('',(#2429),#1840,.T.);
#12797=ADVANCED_FACE('',(#2430),#1841,.T.);
#12798=ADVANCED_FACE('',(#2431),#1842,.T.);
#12799=ADVANCED_FACE('',(#2432,#1448,#1449,#1450),#1843,.T.);
#12800=ADVANCED_FACE('',(#2433,#1451,#1452,#1453),#1844,.F.);
#13294=CLOSED_SHELL('',(#12788,#12789,#12790,#12791,#12792,#12793,#12794,
#12795,#12796,#12797,#12798,#12799,#12800));
#15309=AXIS2_PLACEMENT_3D('',#22628,#18331,#18332);
#15310=AXIS2_PLACEMENT_3D('',#22629,#18333,#18334);
#15311=AXIS2_PLACEMENT_3D('',#22631,#18335,#18336);
#15312=AXIS2_PLACEMENT_3D('',#22634,#18338,#18339);
#15313=AXIS2_PLACEMENT_3D('',#22635,#18340,#18341);
#15314=AXIS2_PLACEMENT_3D('',#22637,#18342,#18343);
#15315=AXIS2_PLACEMENT_3D('',#22638,#18344,#18345);
#15316=AXIS2_PLACEMENT_3D('',#22640,#18346,#18347);
#15317=AXIS2_PLACEMENT_3D('',#22643,#18349,#18350);
#15318=AXIS2_PLACEMENT_3D('',#22644,#18351,#18352);
#15319=AXIS2_PLACEMENT_3D('',#22646,#18353,#18354);
#15320=AXIS2_PLACEMENT_3D('',#22647,#18355,#18356);
#15321=AXIS2_PLACEMENT_3D('',#22649,#18357,#18358);
#15322=AXIS2_PLACEMENT_3D('',#22652,#18360,#18361);
#15323=AXIS2_PLACEMENT_3D('',#22653,#18362,#18363);
#15324=AXIS2_PLACEMENT_3D('',#22656,#18365,#18366);
#15325=AXIS2_PLACEMENT_3D('',#22657,#18367,#18368);
#15326=AXIS2_PLACEMENT_3D('',#22660,#18370,#18371);
#15327=AXIS2_PLACEMENT_3D('',#22661,#18372,#18373);
#15328=AXIS2_PLACEMENT_3D('',#22670,#18378,#18379);
#15329=AXIS2_PLACEMENT_3D('',#22676,#18383,#18384);
#15330=AXIS2_PLACEMENT_3D('',#22682,#18388,#18389);
#15331=AXIS2_PLACEMENT_3D('',#22685,#18392,#18393);
#15332=AXIS2_PLACEMENT_3D('',#22686,#18394,#18395);
#18331=DIRECTION('axis',(0.,0.,1.));
#18332=DIRECTION('refdir',(1.,0.,0.));
#18333=DIRECTION('center_axis',(1.,0.,0.));
#18334=DIRECTION('ref_axis',(0.,0.,-1.));
#18335=DIRECTION('center_axis',(1.,0.,0.));
#18336=DIRECTION('ref_axis',(0.,0.,-1.));
#18337=DIRECTION('',(-1.,0.,0.));
#18338=DIRECTION('center_axis',(1.,0.,0.));
#18339=DIRECTION('ref_axis',(0.,0.,-1.));
#18340=DIRECTION('center_axis',(1.,0.,0.));
#18341=DIRECTION('ref_axis',(0.,0.,-1.));
#18342=DIRECTION('center_axis',(-1.,0.,0.));
#18343=DIRECTION('ref_axis',(0.,0.,-1.));
#18344=DIRECTION('center_axis',(1.,0.,0.));
#18345=DIRECTION('ref_axis',(0.,0.,-1.));
#18346=DIRECTION('center_axis',(1.,0.,0.));
#18347=DIRECTION('ref_axis',(0.,0.,-1.));
#18348=DIRECTION('',(-1.,0.,0.));
#18349=DIRECTION('center_axis',(1.,0.,0.));
#18350=DIRECTION('ref_axis',(0.,0.,-1.));
#18351=DIRECTION('center_axis',(1.,0.,0.));
#18352=DIRECTION('ref_axis',(0.,0.,-1.));
#18353=DIRECTION('center_axis',(-1.,0.,0.));
#18354=DIRECTION('ref_axis',(0.,0.,-1.));
#18355=DIRECTION('center_axis',(1.,0.,0.));
#18356=DIRECTION('ref_axis',(0.,0.,-1.));
#18357=DIRECTION('center_axis',(1.,0.,0.));
#18358=DIRECTION('ref_axis',(0.,0.,-1.));
#18359=DIRECTION('',(1.,0.,0.));
#18360=DIRECTION('center_axis',(-1.,0.,0.));
#18361=DIRECTION('ref_axis',(0.,0.,-1.));
#18362=DIRECTION('center_axis',(1.,0.,0.));
#18363=DIRECTION('ref_axis',(0.,0.,-1.));
#18364=DIRECTION('',(1.,0.,0.));
#18365=DIRECTION('center_axis',(-1.,0.,0.));
#18366=DIRECTION('ref_axis',(0.,0.,-1.));
#18367=DIRECTION('center_axis',(1.,0.,0.));
#18368=DIRECTION('ref_axis',(0.,0.,-1.));
#18369=DIRECTION('',(1.,0.,0.));
#18370=DIRECTION('center_axis',(-1.,0.,0.));
#18371=DIRECTION('ref_axis',(0.,0.,-1.));
#18372=DIRECTION('center_axis',(0.,0.,1.));
#18373=DIRECTION('ref_axis',(0.,-1.,0.));
#18374=DIRECTION('',(0.,-1.,0.));
#18375=DIRECTION('',(1.,0.,0.));
#18376=DIRECTION('',(0.,-1.,0.));
#18377=DIRECTION('',(1.,0.,0.));
#18378=DIRECTION('center_axis',(0.,1.,0.));
#18379=DIRECTION('ref_axis',(0.,0.,1.));
#18380=DIRECTION('',(0.,0.,1.));
#18381=DIRECTION('',(0.,0.,1.));
#18382=DIRECTION('',(1.,0.,0.));
#18383=DIRECTION('center_axis',(0.,0.,-1.));
#18384=DIRECTION('ref_axis',(0.,1.,0.));
#18385=DIRECTION('',(0.,1.,0.));
#18386=DIRECTION('',(0.,1.,0.));
#18387=DIRECTION('',(1.,0.,0.));
#18388=DIRECTION('center_axis',(0.,-1.,0.));
#18389=DIRECTION('ref_axis',(0.,0.,-1.));
#18390=DIRECTION('',(0.,0.,-1.));
#18391=DIRECTION('',(0.,0.,-1.));
#18392=DIRECTION('center_axis',(1.,0.,0.));
#18393=DIRECTION('ref_axis',(0.,0.,-1.));
#18394=DIRECTION('center_axis',(1.,0.,0.));
#18395=DIRECTION('ref_axis',(0.,0.,-1.));
#22628=CARTESIAN_POINT('',(0.,0.,0.));
#22629=CARTESIAN_POINT('Origin',(40.22983346,3.,16.));
#22630=CARTESIAN_POINT('',(40.42983346,3.,17.04));
#22631=CARTESIAN_POINT('Origin',(40.42983346,3.,16.));
#22632=CARTESIAN_POINT('',(40.22983346,3.,17.04));
#22633=CARTESIAN_POINT('',(40.22983346,3.,17.04));
#22634=CARTESIAN_POINT('Origin',(40.22983346,3.,16.));
#22635=CARTESIAN_POINT('Origin',(40.22983346,3.,16.));
#22636=CARTESIAN_POINT('',(40.22983346,3.,16.8));
#22637=CARTESIAN_POINT('Origin',(40.22983346,3.,16.));
#22638=CARTESIAN_POINT('Origin',(40.22983346,-3.,16.));
#22639=CARTESIAN_POINT('',(40.42983346,-3.,17.04));
#22640=CARTESIAN_POINT('Origin',(40.42983346,-3.,16.));
#22641=CARTESIAN_POINT('',(40.22983346,-3.,17.04));
#22642=CARTESIAN_POINT('',(40.22983346,-3.,17.04));
#22643=CARTESIAN_POINT('Origin',(40.22983346,-3.,16.));
#22644=CARTESIAN_POINT('Origin',(40.22983346,-3.,16.));
#22645=CARTESIAN_POINT('',(40.22983346,-3.,16.8));
#22646=CARTESIAN_POINT('Origin',(40.22983346,-3.,16.));
#22647=CARTESIAN_POINT('Origin',(40.32983346,0.,16.));
#22648=CARTESIAN_POINT('',(40.42983346,-7.9602041944578E-17,16.65));
#22649=CARTESIAN_POINT('Origin',(40.42983346,0.,16.));
#22650=CARTESIAN_POINT('',(40.62983346,7.9602041944578E-17,16.65));
#22651=CARTESIAN_POINT('',(40.32983346,-7.9602041944578E-17,16.65));
#22652=CARTESIAN_POINT('Origin',(40.62983346,0.,16.));
#22653=CARTESIAN_POINT('Origin',(40.32983346,-3.,16.));
#22654=CARTESIAN_POINT('',(40.62983346,-3.,16.8));
#22655=CARTESIAN_POINT('',(40.32983346,-3.,16.8));
#22656=CARTESIAN_POINT('Origin',(40.62983346,-3.,16.));
#22657=CARTESIAN_POINT('Origin',(40.32983346,3.,16.));
#22658=CARTESIAN_POINT('',(40.62983346,3.,16.8));
#22659=CARTESIAN_POINT('',(40.32983346,3.,16.8));
#22660=CARTESIAN_POINT('Origin',(40.62983346,3.,16.));
#22661=CARTESIAN_POINT('Origin',(40.42983346,4.7,17.7));
#22662=CARTESIAN_POINT('',(40.42983346,4.7,17.7));
#22663=CARTESIAN_POINT('',(40.42983346,-4.3,17.7));
#22664=CARTESIAN_POINT('',(40.42983346,4.7,17.7));
#22665=CARTESIAN_POINT('',(40.62983346,-4.3,17.7));
#22666=CARTESIAN_POINT('',(40.42983346,-4.3,17.7));
#22667=CARTESIAN_POINT('',(40.62983346,4.7,17.7));
#22668=CARTESIAN_POINT('',(40.62983346,4.7,17.7));
#22669=CARTESIAN_POINT('',(40.42983346,4.7,17.7));
#22670=CARTESIAN_POINT('Origin',(40.42983346,4.7,14.3));
#22671=CARTESIAN_POINT('',(40.42983346,4.7,14.3));
#22672=CARTESIAN_POINT('',(40.42983346,4.7,14.3));
#22673=CARTESIAN_POINT('',(40.62983346,4.7,14.3));
#22674=CARTESIAN_POINT('',(40.62983346,4.7,14.3));
#22675=CARTESIAN_POINT('',(40.42983346,4.7,14.3));
#22676=CARTESIAN_POINT('Origin',(40.42983346,-4.3,14.3));
#22677=CARTESIAN_POINT('',(40.42983346,-4.3,14.3));
#22678=CARTESIAN_POINT('',(40.42983346,-4.3,14.3));
#22679=CARTESIAN_POINT('',(40.62983346,-4.3,14.3));
#22680=CARTESIAN_POINT('',(40.62983346,-4.3,14.3));
#22681=CARTESIAN_POINT('',(40.42983346,-4.3,14.3));
#22682=CARTESIAN_POINT('Origin',(40.42983346,-4.3,17.7));
#22683=CARTESIAN_POINT('',(40.42983346,-4.3,17.7));
#22684=CARTESIAN_POINT('',(40.62983346,-4.3,17.7));
#22685=CARTESIAN_POINT('Origin',(40.62983346,0.2,16.));
#22686=CARTESIAN_POINT('Origin',(40.42983346,0.2,16.));
#24908=UNCERTAINTY_MEASURE_WITH_UNIT(LENGTH_MEASURE(0.001),#25101,
'DISTANCE_ACCURACY_VALUE',
'Maximum model space distance between geometric entities at asserted c
onnectivities');
#24979=UNCERTAINTY_MEASURE_WITH_UNIT(LENGTH_MEASURE(0.001),#25101,
'DISTANCE_ACCURACY_VALUE',
'Maximum model space distance between geometric entities at asserted c
onnectivities');
#25029=(
GEOMETRIC_REPRESENTATION_CONTEXT(3)
GLOBAL_UNCERTAINTY_ASSIGNED_CONTEXT((#24908))
GLOBAL_UNIT_ASSIGNED_CONTEXT((#25101,#25103,#25104))
REPRESENTATION_CONTEXT('','3D')
);
#25100=(
GEOMETRIC_REPRESENTATION_CONTEXT(3)
GLOBAL_UNCERTAINTY_ASSIGNED_CONTEXT((#24979))
GLOBAL_UNIT_ASSIGNED_CONTEXT((#25101,#25103,#25104))
REPRESENTATION_CONTEXT('','3D')
);
#25101=(
LENGTH_UNIT()
NAMED_UNIT(*)
SI_UNIT(.CENTI.,.METRE.)
);
#25103=(
NAMED_UNIT(*)
PLANE_ANGLE_UNIT()
SI_UNIT($,.RADIAN.)
);
#25104=(
NAMED_UNIT(*)
SI_UNIT($,.STERADIAN.)
SOLID_ANGLE_UNIT()
);
#25154=SHAPE_DEFINITION_REPRESENTATION(#25274,#25559);
#25274=PRODUCT_DEFINITION_SHAPE('',$,#25680);
#25559=SHAPE_REPRESENTATION('',(#15309),#25029);
#25630=PRODUCT_DEFINITION_CONTEXT('part definition',#25992,'design');
#25680=PRODUCT_DEFINITION('Linear bearing keeper (3)',
'Linear bearing keeper (3)',#25800,#25630);
#25800=PRODUCT_DEFINITION_FORMATION('',$,#26043);
#25992=APPLICATION_CONTEXT(
'Core Data for Automotive Mechanical Design Process');
#25993=PRODUCT_CONTEXT('part definition',#25992,'mechanical');
#26043=PRODUCT('Linear bearing keeper (3)','Linear bearing keeper (3)',
'Linear bearing keeper (3)',(#25993));
#26185=COLOUR_RGB('Grey',0.48,0.52,0.57);
#26186=FILL_AREA_STYLE_COLOUR('',#26185);
#26187=FILL_AREA_STYLE('',(#26186));
#26188=SURFACE_STYLE_FILL_AREA(#26187);
#26189=SURFACE_SIDE_STYLE('',(#26188));
#26190=SURFACE_STYLE_USAGE(.BOTH.,#26189);
#26191=PRESENTATION_STYLE_ASSIGNMENT((#26190));
ENDSEC;
END-ISO-10303-21;
